ISO-10303-21;
HEADER;
/* Generated by software containing ST-Developer
 * from STEP Tools, Inc. (www.steptools.com) 
 */

FILE_DESCRIPTION(
/* description */ ('Counterbalanced vertical column'),
/* implementation_level */ '2;1');

FILE_NAME(
/* name */ 'Flat Washer - M5.step',
/* time_stamp */ '2026-10-29T16:47:22-07:00',
/* author */ (''),
/* organization */ (''),
/* preprocessor_version */ 'ST-DEVELOPER v20.2',
/* originating_system */ 'Autodesk Translation Framework v15.17.0.0',
/* authorisation */ '');

FILE_SCHEMA (('AUTOMOTIVE_DESIGN { 1 0 10303 214 3 1 1 }'));
ENDSEC;

DATA;
#10=MECHANICAL_DESIGN_GEOMETRIC_PRESENTATION_REPRESENTATION('',(#372),#15040);
#254=CONICAL_SURFACE('',#7921,0.275,0.785398163397449);
#302=SHAPE_REPRESENTATION_RELATIONSHIP('SRR','None',#15206,#337);
#337=ADVANCED_BREP_SHAPE_REPRESENTATION('',(#405),#15025);
#372=STYLED_ITEM('',(#15464),#405);
#405=MANIFOLD_SOLID_BREP('Body1',#7097);
#496=FACE_BOUND('',#1572,.T.);
#497=FACE_BOUND('',#1575,.T.);
#719=PLANE('',#7926);
#720=PLANE('',#7930);
#1084=FACE_OUTER_BOUND('',#1569,.T.);
#1085=FACE_OUTER_BOUND('',#1570,.T.);
#1086=FACE_OUTER_BOUND('',#1571,.T.);
#1087=FACE_OUTER_BOUND('',#1573,.T.);
#1088=FACE_OUTER_BOUND('',#1574,.T.);
#1569=EDGE_LOOP('',(#5914,#5915,#5916,#5917));
#1570=EDGE_LOOP('',(#5918,#5919,#5920,#5921));
#1571=EDGE_LOOP('',(#5922));
#1572=EDGE_LOOP('',(#5923));
#1573=EDGE_LOOP('',(#5924,#5925,#5926,#5927));
#1574=EDGE_LOOP('',(#5928));
#1575=EDGE_LOOP('',(#5929));
#2172=LINE('',#14199,#2843);
#2173=LINE('',#14203,#2844);
#2174=LINE('',#14210,#2845);
#2843=VECTOR('',#9492,0.275);
#2844=VECTOR('',#9497,0.265);
#2845=VECTOR('',#9506,0.5);
#3226=CIRCLE('',#7922,0.285);
#3227=CIRCLE('',#7923,0.265);
#3228=CIRCLE('',#7925,0.265);
#3229=CIRCLE('',#7927,0.5);
#3230=CIRCLE('',#7929,0.5);
#3679=VERTEX_POINT('',#14196);
#3680=VERTEX_POINT('',#14198);
#3681=VERTEX_POINT('',#14202);
#3682=VERTEX_POINT('',#14206);
#3683=VERTEX_POINT('',#14209);
#4458=EDGE_CURVE('',#3679,#3679,#3226,.T.);
#4459=EDGE_CURVE('',#3679,#3680,#2172,.T.);
#4460=EDGE_CURVE('',#3680,#3680,#3227,.T.);
#4461=EDGE_CURVE('',#3680,#3681,#2173,.T.);
#4462=EDGE_CURVE('',#3681,#3681,#3228,.T.);
#4463=EDGE_CURVE('',#3682,#3682,#3229,.T.);
#4464=EDGE_CURVE('',#3682,#3683,#2174,.T.);
#4465=EDGE_CURVE('',#3683,#3683,#3230,.T.);
#5914=ORIENTED_EDGE('',*,*,#4458,.T.);
#5915=ORIENTED_EDGE('',*,*,#4459,.T.);
#5916=ORIENTED_EDGE('',*,*,#4460,.T.);
#5917=ORIENTED_EDGE('',*,*,#4459,.F.);
#5918=ORIENTED_EDGE('',*,*,#4460,.F.);
#5919=ORIENTED_EDGE('',*,*,#4461,.T.);
#5920=ORIENTED_EDGE('',*,*,#4462,.T.);
#5921=ORIENTED_EDGE('',*,*,#4461,.F.);
#5922=ORIENTED_EDGE('',*,*,#4463,.T.);
#5923=ORIENTED_EDGE('',*,*,#4458,.F.);
#5924=ORIENTED_EDGE('',*,*,#4463,.F.);
#5925=ORIENTED_EDGE('',*,*,#4464,.T.);
#5926=ORIENTED_EDGE('',*,*,#4465,.T.);
#5927=ORIENTED_EDGE('',*,*,#4464,.F.);
#5928=ORIENTED_EDGE('',*,*,#4465,.F.);
#5929=ORIENTED_EDGE('',*,*,#4462,.F.);
#6636=CYLINDRICAL_SURFACE('',#7924,0.265);
#6637=CYLINDRICAL_SURFACE('',#7928,0.5);
#6926=ADVANCED_FACE('',(#1084),#254,.F.);
#6927=ADVANCED_FACE('',(#1085),#6636,.F.);
#6928=ADVANCED_FACE('',(#1086,#496),#719,.T.);
#6929=ADVANCED_FACE('',(#1087),#6637,.T.);
#6930=ADVANCED_FACE('',(#1088,#497),#720,.F.);
#7097=CLOSED_SHELL('',(#6926,#6927,#6928,#6929,#6930));
#7920=AXIS2_PLACEMENT_3D('',#14194,#9486,#9487);
#7921=AXIS2_PLACEMENT_3D('',#14195,#9488,#9489);
#7922=AXIS2_PLACEMENT_3D('',#14197,#9490,#9491);
#7923=AXIS2_PLACEMENT_3D('',#14200,#9493,#9494);
#7924=AXIS2_PLACEMENT_3D('',#14201,#9495,#9496);
#7925=AXIS2_PLACEMENT_3D('',#14204,#9498,#9499);
#7926=AXIS2_PLACEMENT_3D('',#14205,#9500,#9501);
#7927=AXIS2_PLACEMENT_3D('',#14207,#9502,#9503);
#7928=AXIS2_PLACEMENT_3D('',#14208,#9504,#9505);
#7929=AXIS2_PLACEMENT_3D('',#14211,#9507,#9508);
#7930=AXIS2_PLACEMENT_3D('',#14212,#9509,#9510);
#9486=DIRECTION('axis',(0.,0.,1.));
#9487=DIRECTION('refdir',(1.,0.,0.));
#9488=DIRECTION('center_axis',(0.,1.,0.));
#9489=DIRECTION('ref_axis',(1.,0.,0.));
#9490=DIRECTION('center_axis',(0.,1.,0.));
#9491=DIRECTION('ref_axis',(1.,0.,0.));
#9492=DIRECTION('',(0.707106781186548,-0.707106781186547,-8.65956056235494E-17));
#9493=DIRECTION('center_axis',(0.,-1.,0.));
#9494=DIRECTION('ref_axis',(1.,0.,0.));
#9495=DIRECTION('center_axis',(0.,1.,0.));
#9496=DIRECTION('ref_axis',(1.,0.,0.));
#9497=DIRECTION('',(0.,-1.,0.));
#9498=DIRECTION('center_axis',(0.,-1.,0.));
#9499=DIRECTION('ref_axis',(1.,0.,0.));
#9500=DIRECTION('center_axis',(0.,1.,0.));
#9501=DIRECTION('ref_axis',(1.,0.,0.));
#9502=DIRECTION('center_axis',(0.,1.,0.));
#9503=DIRECTION('ref_axis',(1.,0.,0.));
#9504=DIRECTION('center_axis',(0.,1.,0.));
#9505=DIRECTION('ref_axis',(1.,0.,0.));
#9506=DIRECTION('',(0.,-1.,0.));
#9507=DIRECTION('center_axis',(0.,1.,0.));
#9508=DIRECTION('ref_axis',(1.,0.,0.));
#9509=DIRECTION('center_axis',(0.,1.,0.));
#9510=DIRECTION('ref_axis',(1.,0.,0.));
#14194=CARTESIAN_POINT('',(0.,0.,0.));
#14195=CARTESIAN_POINT('Origin',(0.,0.09,0.));
#14196=CARTESIAN_POINT('',(-0.285,0.1,3.49024337756996E-17));
#14197=CARTESIAN_POINT('Origin',(0.,0.1,0.));
#14198=CARTESIAN_POINT('',(-0.265,0.08,-3.24531401774049E-17));
#14199=CARTESIAN_POINT('',(-0.275,0.09,3.36777869765522E-17));
#14200=CARTESIAN_POINT('Origin',(0.,0.08,0.));
#14201=CARTESIAN_POINT('Origin',(0.,0.,0.));
#14202=CARTESIAN_POINT('',(-0.265,0.,3.24531401774049E-17));
#14203=CARTESIAN_POINT('',(-0.265,0.,3.24531401774049E-17));
#14204=CARTESIAN_POINT('Origin',(0.,0.,0.));
#14205=CARTESIAN_POINT('Origin',(0.,0.1,0.));
#14206=CARTESIAN_POINT('',(-0.5,0.1,6.12323399573677E-17));
#14207=CARTESIAN_POINT('Origin',(0.,0.1,0.));
#14208=CARTESIAN_POINT('Origin',(0.,0.,0.));
#14209=CARTESIAN_POINT('',(-0.5,0.,6.12323399573677E-17));
#14210=CARTESIAN_POINT('',(-0.5,0.,6.12323399573677E-17));
#14211=CARTESIAN_POINT('Origin',(0.,0.,0.));
#14212=CARTESIAN_POINT('Origin',(0.,0.,0.));
#14985=UNCERTAINTY_MEASURE_WITH_UNIT(LENGTH_MEASURE(0.001),#15041,
'DISTANCE_ACCURACY_VALUE',
'Maximum model space distance between geometric entities at asserted c
onnectivities');
#15000=UNCERTAINTY_MEASURE_WITH_UNIT(LENGTH_MEASURE(0.001),#15041,
'DISTANCE_ACCURACY_VALUE',
'Maximum model space distance between geometric entities at asserted c
onnectivities');
#15025=(
GEOMETRIC_REPRESENTATION_CONTEXT(3)
GLOBAL_UNCERTAINTY_ASSIGNED_CONTEXT((#14985))
GLOBAL_UNIT_ASSIGNED_CONTEXT((#15041,#15043,#15044))
REPRESENTATION_CONTEXT('','3D')
);
#15040=(
GEOMETRIC_REPRESENTATION_CONTEXT(3)
GLOBAL_UNCERTAINTY_ASSIGNED_CONTEXT((#15000))
GLOBAL_UNIT_ASSIGNED_CONTEXT((#15041,#15043,#15044))
REPRESENTATION_CONTEXT('','3D')
);
#15041=(
LENGTH_UNIT()
NAMED_UNIT(*)
SI_UNIT(.CENTI.,.METRE.)
);
#15043=(
NAMED_UNIT(*)
PLANE_ANGLE_UNIT()
SI_UNIT($,.RADIAN.)
);
#15044=(
NAMED_UNIT(*)
SI_UNIT($,.STERADIAN.)
SOLID_ANGLE_UNIT()
);
#15069=SHAPE_DEFINITION_REPRESENTATION(#15108,#15206);
#15108=PRODUCT_DEFINITION_SHAPE('',$,#15246);
#15206=SHAPE_REPRESENTATION('',(#7920),#15025);
#15221=PRODUCT_DEFINITION_CONTEXT('part definition',#15340,'design');
#15246=PRODUCT_DEFINITION('Flat Washer - M5','Flat Washer - M5',#15285,
#15221);
#15285=PRODUCT_DEFINITION_FORMATION('',$,#15366);
#15340=APPLICATION_CONTEXT(
'Core Data for Automotive Mechanical Design Process');
#15341=PRODUCT_CONTEXT('part definition',#15340,'mechanical');
#15366=PRODUCT('Flat Washer - M5','Flat Washer - M5','Flat Washer - M5',
(#15341));
#15458=COLOUR_RGB('Black',0.12,0.14,0.17);
#15459=FILL_AREA_STYLE_COLOUR('',#15458);
#15460=FILL_AREA_STYLE('',(#15459));
#15461=SURFACE_STYLE_FILL_AREA(#15460);
#15462=SURFACE_SIDE_STYLE('',(#15461));
#15463=SURFACE_STYLE_USAGE(.BOTH.,#15462);
#15464=PRESENTATION_STYLE_ASSIGNMENT((#15463));
ENDSEC;
END-ISO-10303-21;
